ISO-10303-21;
HEADER;
FILE_DESCRIPTION (('STEP AP214'),
    '1' );
FILE_NAME ('radial ball bearing_68_iso_ISO 15 RBB - 3025 - 14,SI,NC,14_68.step',
    '2026-10-08T09:53:37',
    ( '' ),
    ( '' ),
    'SwSTEP 2.0',
    'SolidWorks 2026',
    '' );
FILE_SCHEMA (( 'AUTOMOTIVE_DESIGN' ));
ENDSEC;

DATA;
#34=DIRECTION ( 'NONE',  ( -8.783410004945701396E-16, -1.065814103640131188E-14, -1.000000000000000000 ) ) ;
#140=AXIS2_PLACEMENT_3D ( 'NONE', #41358, #52630, #1547 ) ;
#177=CYLINDRICAL_SURFACE ( 'NONE', #69251, 20.20000000000036522 ) ;
#326=MECHANICAL_DESIGN_GEOMETRIC_PRESENTATION_REPRESENTATION('',(#21897),#73467);
#392=ADVANCED_FACE ( 'NONE', ( #21114 ), #31659, .T. ) ;
#615=ORIENTED_EDGE ( 'NONE', *, *, #59441, .T. ) ;
#624=ADVANCED_FACE ( 'NONE', ( #40645, #51552 ), #36846, .T. ) ;
#707=ORIENTED_EDGE ( 'NONE', *, *, #65946, .T. ) ;
#801=ORIENTED_EDGE ( 'NONE', *, *, #36762, .T. ) ;
#825=AXIS2_PLACEMENT_3D ( 'NONE', #17122, #51706, #44594 ) ;
#843=DIRECTION ( 'NONE',  ( 1.000000000000000000, 1.427937372958405461E-15, 7.962523111839130290E-16 ) ) ;
#1114=CARTESIAN_POINT ( 'NONE',  ( 8.000000000000007105, 1.142349898368116708E-14, 6.370018489481387452E-15 ) ) ;
#1176=EDGE_CURVE ( 'NONE', #54538, #68921, #7226, .T. ) ;
#1422=EDGE_LOOP ( 'NONE', ( #60315, #40508, #7746, #707 ) ) ;
#1457=AXIS2_PLACEMENT_3D ( 'NONE', #5326, #47014, #69566 ) ;
#1459=EDGE_LOOP ( 'NONE', ( #69912, #42166 ) ) ;
#1547=DIRECTION ( 'NONE',  ( -7.945298363252408085E-16, -1.065814103640131188E-14, -1.000000000000000000 ) ) ;
#1608=ORIENTED_EDGE ( 'NONE', *, *, #37255, .T. ) ;
#1645=CARTESIAN_POINT ( 'NONE',  ( -20.63750000000001705, -1.978676859095576340E-13, -15.80000000000029914 ) ) ;
#1709=ORIENTED_EDGE ( 'NONE', *, *, #54143, .F. ) ;
#1883=ORIENTED_EDGE ( 'NONE', *, *, #40336, .T. ) ;
#1917=EDGE_LOOP ( 'NONE', ( #19140, #20873 ) ) ;
#1944=DIRECTION ( 'NONE',  ( -7.685483754327489091E-16, -1.065814103640131188E-14, -1.000000000000000000 ) ) ;
#1992=DIRECTION ( 'NONE',  ( 1.000000000000000000, 1.427937372958405461E-15, 7.962523111839130290E-16 ) ) ;
#2117=DIRECTION ( 'NONE',  ( 1.000000000000000000, 1.427937372958405461E-15, 7.962523111839130290E-16 ) ) ;
#2336=CIRCLE ( 'NONE', #22757, 0.5999999999999928724 ) ;
#2345=CARTESIAN_POINT ( 'NONE',  ( 7.399999999999994138, 1.489868709406086122E-13, 12.50000000000000533 ) ) ;
#2375=AXIS2_PLACEMENT_3D ( 'NONE', #49526, #60099, #66104 ) ;
#2406=DIRECTION ( 'NONE',  ( -7.945298363252408085E-16, -1.065814103640131188E-14, -1.000000000000000000 ) ) ;
#2469=CARTESIAN_POINT ( 'NONE',  ( -7.400000000000014566, -1.501883841367401167E-13, -13.10000000000024123 ) ) ;
#2850=FACE_OUTER_BOUND ( 'NONE', #1422, .T. ) ;
#2966=ORIENTED_EDGE ( 'NONE', *, *, #71220, .T. ) ;
#3056=DIRECTION ( 'NONE',  ( -7.728965982074743403E-16, -1.065814103640131346E-14, -1.000000000000000000 ) ) ;
#3128=DIRECTION ( 'NONE',  ( 1.000000000000000000, 1.427937372958405461E-15, 7.962523111839130290E-16 ) ) ;
#3168=DIRECTION ( 'NONE',  ( 1.000000000000000000, 1.427937372958405461E-15, 7.962523111839130290E-16 ) ) ;
#3418=DIRECTION ( 'NONE',  ( 1.000000000000000000, 1.427937372958405461E-15, 7.962523111839130290E-16 ) ) ;
#3484=LINE ( 'NONE', #7994, #39798 ) ;
#3501=TOROIDAL_SURFACE ( 'NONE', #49085, 18.00000000000000000, 3.300000000000000266 ) ;
#3509=FACE_BOUND ( 'NONE', #1459, .T. ) ;
#3522=AXIS2_PLACEMENT_3D ( 'NONE', #57326, #53167, #34384 ) ;
#3776=DIRECTION ( 'NONE',  ( 1.000000000000000000, 1.427937372958405461E-15, 7.962523111839130290E-16 ) ) ;
#3784=DIRECTION ( 'NONE',  ( 7.962523111839282146E-16, -1.065814103640130873E-14, -1.000000000000000000 ) ) ;
#3888=COLOUR_RGB ( '', 0.08235294, 0.09019608, 0.10196078) ;
#4089=SURFACE_SIDE_STYLE ('',( #9707 ) ) ;
#4171=DIRECTION ( 'NONE',  ( 0.000000000000000000, 1.053567635648656885E-14, 1.000000000000000000 ) ) ;
#4336=EDGE_CURVE ( 'NONE', #22617, #32997, #35008, .T. ) ;
#4373=EDGE_LOOP ( 'NONE', ( #40029, #34840, #1883, #44041 ) ) ;
#4425=ADVANCED_FACE ( 'NONE', ( #22601, #45547 ), #5690, .T. ) ;
#4473=ORIENTED_EDGE ( 'NONE', *, *, #49381, .T. ) ;
#4520=AXIS2_PLACEMENT_3D ( 'NONE', #62533, #11009, #73406 ) ;
#4815=CARTESIAN_POINT ( 'NONE',  ( -7.400000000000013678, -1.437934995148992251E-13, -12.50000000000023093 ) ) ;
#5069=FACE_OUTER_BOUND ( 'NONE', #24527, .T. ) ;
#5136=DIRECTION ( 'NONE',  ( 1.000000000000000000, 1.427937372958405461E-15, 7.962523111839130290E-16 ) ) ;
#5290=DIRECTION ( 'NONE',  ( -7.962523111839282146E-16, 1.065814103640130873E-14, 1.000000000000000000 ) ) ;
#5326=CARTESIAN_POINT ( 'NONE',  ( -8.000000000000007105, 20.20000000000007390, 2.076830587532255432E-13 ) ) ;
#5344=DIRECTION ( 'NONE',  ( -8.587739980083048116E-16, -1.065814103640131346E-14, -1.000000000000000000 ) ) ;
#5372=FACE_OUTER_BOUND ( 'NONE', #50172, .T. ) ;
#5422=AXIS2_PLACEMENT_3D ( 'NONE', #20026, #49343, #42981 ) ;
#5690=PLANE ( 'NONE',  #1457 ) ;
#5714=DIRECTION ( 'NONE',  ( -8.783410004945701396E-16, -1.065814103640131188E-14, -1.000000000000000000 ) ) ;
#5715=CARTESIAN_POINT ( 'NONE',  ( -20.63749999999999574, -2.946905753440916183E-14, -1.643265707205091412E-14 ) ) ;
#5840=ORIENTED_EDGE ( 'NONE', *, *, #47459, .T. ) ;
#5887=EDGE_CURVE ( 'NONE', #40700, #59084, #59613, .T. ) ;
#6198=AXIS2_PLACEMENT_3D ( 'NONE', #66606, #66963, #38029 ) ;
#6374=FACE_OUTER_BOUND ( 'NONE', #17948, .T. ) ;
#6504=ORIENTED_EDGE ( 'NONE', *, *, #34224, .T. ) ;
#6740=DIRECTION ( 'NONE',  ( -1.427937372958396981E-15, 1.000000000000000000, -1.053567635648657358E-14 ) ) ;
#6758=ORIENTED_EDGE ( 'NONE', *, *, #54065, .F. ) ;
#6812=DIRECTION ( 'NONE',  ( -7.959965316982041921E-16, -1.065814103640131188E-14, -1.000000000000000000 ) ) ;
#6896=CARTESIAN_POINT ( 'NONE',  ( 7.999999999999991118, 2.252361157298889269E-13, 20.20000000000000995 ) ) ;
#6901=ADVANCED_FACE ( 'NONE', ( #70872 ), #61617, .T. ) ;
#6929=ORIENTED_EDGE ( 'NONE', *, *, #15217, .F. ) ;
#6946=DIRECTION ( 'NONE',  ( 1.000000000000000000, 1.427937372958405461E-15, 7.962523111839130290E-16 ) ) ;
#7022=ADVANCED_FACE ( 'NONE', ( #21210 ), #61662, .T. ) ;
#7072=DIRECTION ( 'NONE',  ( -7.685483754327489091E-16, -1.065814103640131188E-14, -1.000000000000000000 ) ) ;
#7129=ORIENTED_EDGE ( 'NONE', *, *, #4336, .T. ) ;
#7139=ORIENTED_EDGE ( 'NONE', *, *, #8845, .T. ) ;
#7169=CARTESIAN_POINT ( 'NONE',  ( 2.459674775249762302, 3.512261536898573354E-15, 1.958521724562357923E-15 ) ) ;
#7225=ORIENTED_EDGE ( 'NONE', *, *, #13560, .T. ) ;
#7226=CIRCLE ( 'NONE', #16837, 23.50000000000041922 ) ;
#7231=SHAPE_DEFINITION_REPRESENTATION ( #15150, #27826 ) ;
#7406=PRESENTATION_STYLE_ASSIGNMENT (( #35962 ) ) ;
#7663=EDGE_CURVE ( 'NONE', #44464, #59117, #65325, .T. ) ;
#7746=ORIENTED_EDGE ( 'NONE', *, *, #17336, .T. ) ;
#7994=CARTESIAN_POINT ( 'NONE',  ( -20.63750000000001705, -1.978676859095576340E-13, -15.80000000000029914 ) ) ;
#8244=CIRCLE ( 'NONE', #21427, 3.300000000000000711 ) ;
#8291=DIRECTION ( 'NONE',  ( 1.000000000000000000, 1.427937372958405461E-15, 7.962523111839130290E-16 ) ) ;
#8393=CIRCLE ( 'NONE', #50392, 13.10000000000023590 ) ;
#8395=EDGE_CURVE ( 'NONE', #17551, #40700, #70026, .T. ) ;
#8476=CIRCLE ( 'NONE', #18078, 13.10000000000023590 ) ;
#8492=DIRECTION ( 'NONE',  ( -7.962523111839282146E-16, 1.065814103640130873E-14, 1.000000000000000000 ) ) ;
#8649=CARTESIAN_POINT ( 'NONE',  ( -2.459674775249762302, -3.512261536895417911E-15, -1.958521724548552858E-15 ) ) ;
#8845=EDGE_CURVE ( 'NONE', #35626, #46890, #48212, .T. ) ;
#9022=DIRECTION ( 'NONE',  ( 7.962523111839282146E-16, -1.065814103640130873E-14, -1.000000000000000000 ) ) ;
#9030=CARTESIAN_POINT ( 'NONE',  ( 7.400000000000003908, 1.056673655987569448E-14, 5.892267102770835596E-15 ) ) ;
#9072=ORIENTED_EDGE ( 'NONE', *, *, #57148, .F. ) ;
#9130=EDGE_LOOP ( 'NONE', ( #30669, #34625, #1709, #43592 ) ) ;
#9161=CARTESIAN_POINT ( 'NONE',  ( -8.000000000000023093, 2.103003552093192713E-13, 20.19999999999999574 ) ) ;
#9237=ORIENTED_EDGE ( 'NONE', *, *, #33093, .T. ) ;
#9429=CIRCLE ( 'NONE', #61073, 22.90000000000041780 ) ;
#9440=EDGE_LOOP ( 'NONE', ( #28553, #27929, #16855, #18728 ) ) ;
#9541=AXIS2_PLACEMENT_3D ( 'NONE', #27548, #49728, #10628 ) ;
#9567=VERTEX_POINT ( 'NONE', #48686 ) ;
#9595=AXIS2_PLACEMENT_3D ( 'NONE', #12480, #47081, #68899 ) ;
#9707=SURFACE_STYLE_FILL_AREA ( #32625 ) ;
#9808=ORIENTED_EDGE ( 'NONE', *, *, #65190, .F. ) ;
#9839=DIRECTION ( 'NONE',  ( 1.000000000000000000, 1.427937372958405461E-15, 7.962523111839130290E-16 ) ) ;
#9897=AXIS2_PLACEMENT_3D ( 'NONE', #60971, #9839, #32390 ) ;
#9926=FACE_OUTER_BOUND ( 'NONE', #50166, .T. ) ;
#10112=DIRECTION ( 'NONE',  ( -7.728965982074743403E-16, -1.065814103640131346E-14, -1.000000000000000000 ) ) ;
#10202=ORIENTED_EDGE ( 'NONE', *, *, #68598, .F. ) ;
#10628=DIRECTION ( 'NONE',  ( 0.000000000000000000, -1.065814103640131346E-14, -1.000000000000000000 ) ) ;
#10709=EDGE_CURVE ( 'NONE', #73310, #22617, #38346, .T. ) ;
#10800=DIRECTION ( 'NONE',  ( 1.000000000000000000, 1.427937372958405461E-15, 7.962523111839130290E-16 ) ) ;
#11009=DIRECTION ( 'NONE',  ( -1.000000000000000000, -1.427937372958405461E-15, -7.962523111839130290E-16 ) ) ;
#11312=AXIS2_PLACEMENT_3D ( 'NONE', #2469, #71189, #42643 ) ;
#11428=DIRECTION ( 'NONE',  ( -7.962523111839282146E-16, 1.065814103640130873E-14, 1.000000000000000000 ) ) ;
#11628=DIRECTION ( 'NONE',  ( -1.000000000000000000, -1.427937372958405461E-15, -7.962523111839130290E-16 ) ) ;
#11696=DIRECTION ( 'NONE',  ( 1.000000000000000000, 1.427937372958405461E-15, 7.962523111839130290E-16 ) ) ;
#11836=FACE_OUTER_BOUND ( 'NONE', #54127, .T. ) ;
#11863=CIRCLE ( 'NONE', #74292, 20.20000000000036522 ) ;
#12082=CARTESIAN_POINT ( 'NONE',  ( -2.459674775249762302, -3.512261536895417911E-15, -1.958521724548552858E-15 ) ) ;
#12193=ORIENTED_EDGE ( 'NONE', *, *, #71220, .F. ) ;
#12314=DIRECTION ( 'NONE',  ( -1.427937372958396784E-15, 1.000000000000000000, -1.078060571631604545E-14 ) ) ;
#12394=PRODUCT_DEFINITION_FORMATION_WITH_SPECIFIED_SOURCE ( 'ANY', '', #72776, .NOT_KNOWN. ) ;
#12480=CARTESIAN_POINT ( 'NONE',  ( -8.000000000000007105, -1.142349898368590025E-14, -6.370018489464426943E-15 ) ) ;
#12594=ORIENTED_EDGE ( 'NONE', *, *, #36762, .F. ) ;
#12658=SURFACE_STYLE_FILL_AREA ( #58162 ) ;
#12731=ADVANCED_FACE ( 'NONE', ( #5069 ), #27604, .F. ) ;
#12871=CARTESIAN_POINT ( 'NONE',  ( 8.000000000000007105, 1.142349898368116708E-14, 6.370018489481387452E-15 ) ) ;
#12954=EDGE_CURVE ( 'NONE', #68357, #73369, #11863, .T. ) ;
#13130=ORIENTED_EDGE ( 'NONE', *, *, #36913, .F. ) ;
#13169=ADVANCED_FACE ( 'NONE', ( #5372 ), #46685, .F. ) ;
#13468=EDGE_CURVE ( 'NONE', #32997, #22617, #29895, .T. ) ;
#13560=EDGE_CURVE ( 'NONE', #22617, #54538, #30585, .T. ) ;
#13741=ORIENTED_EDGE ( 'NONE', *, *, #17675, .T. ) ;
#13878=EDGE_CURVE ( 'NONE', #14912, #58263, #23951, .T. ) ;
#13916=CARTESIAN_POINT ( 'NONE',  ( 7.399999999999985256, -2.335046931737187547E-13, -22.90000000000041069 ) ) ;
#13978=DIRECTION ( 'NONE',  ( -7.728965982074743403E-16, -1.065814103640131188E-14, -1.000000000000000000 ) ) ;
#14102=CARTESIAN_POINT ( 'NONE',  ( -7.999999999999992895, -1.142349898368590025E-14, -6.370018489464426943E-15 ) ) ;
#14223=( NAMED_UNIT ( * ) PLANE_ANGLE_UNIT ( ) SI_UNIT ( $, .RADIAN. ) );
#14299=CARTESIAN_POINT ( 'NONE',  ( -8.000000000000007105, -1.142349898368590025E-14, -6.370018489464426943E-15 ) ) ;
#14501=EDGE_CURVE ( 'NONE', #49698, #59084, #36438, .T. ) ;
#14552=CARTESIAN_POINT ( 'NONE',  ( -8.000000000000021316, -1.510451465605151834E-13, -13.10000000000024301 ) ) ;
#14646=DIRECTION ( 'NONE',  ( -7.943659481576819828E-16, -1.065814103640131188E-14, -1.000000000000000000 ) ) ;
#14658=CARTESIAN_POINT ( 'NONE',  ( 7.400000000000003908, 1.056673655987569448E-14, 5.892267102770835596E-15 ) ) ;
#14715=EDGE_LOOP ( 'NONE', ( #27363, #35156, #31069, #34452 ) ) ;
#14834=FACE_OUTER_BOUND ( 'NONE', #71842, .T. ) ;
#14912=VERTEX_POINT ( 'NONE', #64567 ) ;
#14916=AXIS2_PLACEMENT_3D ( 'NONE', #42757, #65691, #60071 ) ;
#15150=PRODUCT_DEFINITION_SHAPE ( 'NONE', 'NONE',  #56863 ) ;
#15217=EDGE_CURVE ( 'NONE', #60376, #62960, #64002, .T. ) ;
#15240=APPLICATION_CONTEXT ( 'automotive_design' ) ;
#15270=ORIENTED_EDGE ( 'NONE', *, *, #13878, .F. ) ;
#15319=EDGE_LOOP ( 'NONE', ( #801, #73195 ) ) ;
#15357=AXIS2_PLACEMENT_3D ( 'NONE', #44527, #33596, #73814 ) ;
#15390=CIRCLE ( 'NONE', #52637, 20.20000000000036522 ) ;
#15401=CARTESIAN_POINT ( 'NONE',  ( 7.400000000000014566, 1.517926714436184493E-13, 13.10000000000024123 ) ) ;
#15407=ORIENTED_EDGE ( 'NONE', *, *, #1176, .T. ) ;
#15463=AXIS2_PLACEMENT_3D ( 'NONE', #23743, #57964, #51576 ) ;
#15474=CIRCLE ( 'NONE', #16662, 15.80000000000028315 ) ;
#15481=DIRECTION ( 'NONE',  ( -8.783410004945701396E-16, -1.065814103640131188E-14, -1.000000000000000000 ) ) ;
#15527=CARTESIAN_POINT ( 'NONE',  ( -7.400000000000003908, -1.056673655988042765E-14, -5.892267102755452808E-15 ) ) ;
#15614=VERTEX_POINT ( 'NONE', #52137 ) ;
#15727=ORIENTED_EDGE ( 'NONE', *, *, #5887, .F. ) ;
#15790=AXIS2_PLACEMENT_3D ( 'NONE', #1114, #36373, #7072 ) ;
#15923=ORIENTED_EDGE ( 'NONE', *, *, #34224, .F. ) ;
#15966=CIRCLE ( 'NONE', #66378, 12.50000000000022560 ) ;
#15973=ORIENTED_EDGE ( 'NONE', *, *, #8845, .F. ) ;
#16088=SHAPE_REPRESENTATION_RELATIONSHIP ( 'NONE' , 'NONE' ,  #27826, #47128 ) ;
#16662=AXIS2_PLACEMENT_3D ( 'NONE', #21879, #51933, #30102 ) ;
#16701=CARTESIAN_POINT ( 'NONE',  ( -20.63749999999999574, -2.946905753440916183E-14, -1.643265707205091412E-14 ) ) ;
#16726=CARTESIAN_POINT ( 'NONE',  ( -20.63749999999997797, 2.238751767990224802E-13, 23.50000000000040146 ) ) ;
#16771=AXIS2_PLACEMENT_3D ( 'NONE', #51099, #74023, #51468 ) ;
#16837=AXIS2_PLACEMENT_3D ( 'NONE', #35287, #52947, #29623 ) ;
#16855=ORIENTED_EDGE ( 'NONE', *, *, #48056, .T. ) ;
#17122=CARTESIAN_POINT ( 'NONE',  ( 7.399999999999993250, -1.290549110169840072E-13, -13.10000000000023057 ) ) ;
#17336=EDGE_CURVE ( 'NONE', #68357, #71000, #22013, .T. ) ;
#17439=DIRECTION ( 'NONE',  ( 1.000000000000000000, 1.427937372958405461E-15, 7.962523111839130290E-16 ) ) ;
#17551=VERTEX_POINT ( 'NONE', #9161 ) ;
#17567=FILL_AREA_STYLE_COLOUR ( '', #43005 ) ;
#17675=EDGE_CURVE ( 'NONE', #58263, #67308, #41311, .T. ) ;
#17919=ORIENTED_EDGE ( 'NONE', *, *, #34857, .T. ) ;
#17948=EDGE_LOOP ( 'NONE', ( #71916, #27359, #25876, #60329 ) ) ;
#18078=AXIS2_PLACEMENT_3D ( 'NONE', #30937, #24939, #53515 ) ;
#18232=DIRECTION ( 'NONE',  ( 7.962523111839282146E-16, -1.065814103640130873E-14, -1.000000000000000000 ) ) ;
#18382=ORIENTED_EDGE ( 'NONE', *, *, #7663, .F. ) ;
#18687=EDGE_LOOP ( 'NONE', ( #37980, #29383, #13741, #25335 ) ) ;
#18728=ORIENTED_EDGE ( 'NONE', *, *, #17336, .F. ) ;
#18806=DIRECTION ( 'NONE',  ( 1.000000000000000000, 1.427937372958405461E-15, 7.962523111839130290E-16 ) ) ;
#18862=LINE ( 'NONE', #25987, #23376 ) ;
#19140=ORIENTED_EDGE ( 'NONE', *, *, #36913, .T. ) ;
#19452=AXIS2_PLACEMENT_3D ( 'NONE', #57728, #6946, #18232 ) ;
#19483=CARTESIAN_POINT ( 'NONE',  ( -1.433254160131044044E-14, -1.896421744167617418E-13, -18.00000000000031974 ) ) ;
#19505=CARTESIAN_POINT ( 'NONE',  ( 1.433254160131044044E-14, 1.918465386552270249E-13, 18.00000000000031974 ) ) ;
#19536=EDGE_CURVE ( 'NONE', #59117, #68357, #30560, .T. ) ;
#19586=ORIENTED_EDGE ( 'NONE', *, *, #54065, .T. ) ;
#19716=VECTOR ( 'NONE', #50919, 1000.000000000000000 ) ;
#19735=DIRECTION ( 'NONE',  ( 1.000000000000000000, 0.000000000000000000, 0.000000000000000000 ) ) ;
#19882=EDGE_LOOP ( 'NONE', ( #25597, #17919 ) ) ;
#19923=AXIS2_PLACEMENT_3D ( 'NONE', #26668, #55621, #71046 ) ;
#20026=CARTESIAN_POINT ( 'NONE',  ( 8.000000000000007105, 22.90000000000021885, 2.510511456526457458E-13 ) ) ;
#20261=VECTOR ( 'NONE', #11696, 1000.000000000000000 ) ;
#20474=CIRCLE ( 'NONE', #22903, 0.5999999999999998668 ) ;
#20486=DIRECTION ( 'NONE',  ( 1.000000000000000000, 1.427937372958405461E-15, 7.962523111839130290E-16 ) ) ;
#20531=AXIS2_PLACEMENT_3D ( 'NONE', #63382, #29883, #52837 ) ;
#20681=DIRECTION ( 'NONE',  ( 1.000000000000000000, 1.427937372958405461E-15, 7.962523111839130290E-16 ) ) ;
#20873=ORIENTED_EDGE ( 'NONE', *, *, #15217, .T. ) ;
#20954=ORIENTED_EDGE ( 'NONE', *, *, #44137, .T. ) ;
#21078=ORIENTED_EDGE ( 'NONE', *, *, #62869, .T. ) ;
#21114=FACE_OUTER_BOUND ( 'NONE', #27095, .T. ) ;
#21133=FACE_OUTER_BOUND ( 'NONE', #1917, .T. ) ;
#21210=FACE_OUTER_BOUND ( 'NONE', #4373, .T. ) ;
#21306=EDGE_CURVE ( 'NONE', #17551, #49698, #45873, .T. ) ;
#21427=AXIS2_PLACEMENT_3D ( 'NONE', #61670, #33449, #4171 ) ;
#21482=CARTESIAN_POINT ( 'NONE',  ( -20.63750000000000284, -2.946905753441389499E-14, -1.643265707204933640E-14 ) ) ;
#21502=FACE_OUTER_BOUND ( 'NONE', #14715, .T. ) ;
#21560=LINE ( 'NONE', #28311, #61951 ) ;
#21591=DIRECTION ( 'NONE',  ( -1.000000000000000000, -1.427937372958405461E-15, -7.962523111839130290E-16 ) ) ;
#21662=DIRECTION ( 'NONE',  ( 1.000000000000000000, 1.427937372958405461E-15, 7.962523111839130290E-16 ) ) ;
#21879=CARTESIAN_POINT ( 'NONE',  ( 8.000000000000007105, 1.142349898368116708E-14, 6.370018489481387452E-15 ) ) ;
#21897=STYLED_ITEM ( 'NONE', ( #72835 ), #47128 ) ;
#22013=LINE ( 'NONE', #56980, #54283 ) ;
#22061=EDGE_CURVE ( 'NONE', #9567, #23150, #3484, .T. ) ;
#22138=AXIS2_PLACEMENT_3D ( 'NONE', #60191, #3418, #53782 ) ;
#22312=ORIENTED_EDGE ( 'NONE', *, *, #60687, .F. ) ;
#22396=ORIENTED_EDGE ( 'NONE', *, *, #51865, .F. ) ;
#22601=FACE_BOUND ( 'NONE', #15319, .T. ) ;
#22617=VERTEX_POINT ( 'NONE', #54150 ) ;
#22686=ORIENTED_EDGE ( 'NONE', *, *, #34189, .T. ) ;
#22701=DIRECTION ( 'NONE',  ( 1.000000000000000000, 1.427937372958405461E-15, 7.962523111839130290E-16 ) ) ;
#22757=AXIS2_PLACEMENT_3D ( 'NONE', #13916, #59066, #31219 ) ;
#22780=CARTESIAN_POINT ( 'NONE',  ( 7.400000000000003908, 1.056673655987569448E-14, 5.892267102770835596E-15 ) ) ;
#22903=AXIS2_PLACEMENT_3D ( 'NONE', #47640, #12314, #41268 ) ;
#23003=DIRECTION ( 'NONE',  ( -7.381802025433090153E-16, -1.065814103640131188E-14, -1.000000000000000000 ) ) ;
#23032=EDGE_LOOP ( 'NONE', ( #18382, #43413, #34392, #22312 ) ) ;
#23146=EDGE_LOOP ( 'NONE', ( #59673, #5840, #56798, #67205 ) ) ;
#23150=VERTEX_POINT ( 'NONE', #70083 ) ;
#23225=( NAMED_UNIT ( * ) SI_UNIT ( $, .STERADIAN. ) SOLID_ANGLE_UNIT ( ) );
#23376=VECTOR ( 'NONE', #1992, 1000.000000000000000 ) ;
#23430=FACE_OUTER_BOUND ( 'NONE', #9440, .T. ) ;
#23453=DIRECTION ( 'NONE',  ( 7.943659481576819828E-16, 1.065814103640131188E-14, 1.000000000000000000 ) ) ;
#23593=AXIS2_PLACEMENT_3D ( 'NONE', #8649, #41741, #14646 ) ;
#23743=CARTESIAN_POINT ( 'NONE',  ( -20.63750000000000284, -2.946905753441389499E-14, -1.643265707204933640E-14 ) ) ;
#23789=DIRECTION ( 'NONE',  ( 0.000000000000000000, 1.078060571631605808E-14, 1.000000000000000000 ) ) ;
#23810=CARTESIAN_POINT ( 'NONE',  ( -8.000000000000012434, -2.554949287172803747E-13, -22.90000000000042490 ) ) ;
#23825=AXIS2_PLACEMENT_3D ( 'NONE', #9030, #20681, #3784 ) ;
#23951=CIRCLE ( 'NONE', #63575, 12.50000000000022560 ) ;
#24189=DIRECTION ( 'NONE',  ( 1.000000000000000000, 1.427937372958405461E-15, 7.962523111839130290E-16 ) ) ;
#24442=AXIS2_PLACEMENT_3D ( 'NONE', #14658, #3776, #9022 ) ;
#24527=EDGE_LOOP ( 'NONE', ( #33369, #12594, #59288, #15727 ) ) ;
#24562=AXIS2_PLACEMENT_3D ( 'NONE', #65069, #35376, #59795 ) ;
#24663=EDGE_LOOP ( 'NONE', ( #15923, #22396 ) ) ;
#24716=AXIS2_PLACEMENT_3D ( 'NONE', #71972, #20486, #31750 ) ;
#24939=DIRECTION ( 'NONE',  ( 1.000000000000000000, 1.427937372958405461E-15, 7.962523111839130290E-16 ) ) ;
#25003=CIRCLE ( 'NONE', #47860, 0.5999999999999998668 ) ;
#25032=FACE_OUTER_BOUND ( 'NONE', #50222, .T. ) ;
#25197=DIRECTION ( 'NONE',  ( -1.000000000000000000, -1.427937372958405461E-15, -7.962523111839130290E-16 ) ) ;
#25335=ORIENTED_EDGE ( 'NONE', *, *, #34857, .F. ) ;
#25389=CYLINDRICAL_SURFACE ( 'NONE', #24716, 12.50000000000022560 ) ;
#25597=ORIENTED_EDGE ( 'NONE', *, *, #73348, .T. ) ;
#25744=CARTESIAN_POINT ( 'NONE',  ( -20.63749999999999574, -2.946905753440916183E-14, -1.643265707205091412E-14 ) ) ;
#25871=CARTESIAN_POINT ( 'NONE',  ( -8.000000000000000000, 1.298024359000872731E-13, 13.10000000000022879 ) ) ;
#25876=ORIENTED_EDGE ( 'NONE', *, *, #22061, .T. ) ;
#25901=CARTESIAN_POINT ( 'NONE',  ( -20.63750000000001350, -2.447635064697195611E-13, -20.20000000000038298 ) ) ;
#25987=CARTESIAN_POINT ( 'NONE',  ( -20.63749999999998863, 1.408645127833826896E-13, 15.80000000000026539 ) ) ;
#26059=CARTESIAN_POINT ( 'NONE',  ( -20.63750000000001350, -2.799353718898444395E-13, -23.50000000000043698 ) ) ;
#26064=ORIENTED_EDGE ( 'NONE', *, *, #30691, .F. ) ;
#26183=ORIENTED_EDGE ( 'NONE', *, *, #49381, .F. ) ;
#26251=ORIENTED_EDGE ( 'NONE', *, *, #1176, .F. ) ;
#26414=PLANE ( 'NONE',  #5422 ) ;
#26435=CIRCLE ( 'NONE', #60068, 22.90000000000041780 ) ;
#26635=ADVANCED_FACE ( 'NONE', ( #6374 ), #29278, .T. ) ;
#26668=CARTESIAN_POINT ( 'NONE',  ( -8.000000000000007105, 15.80000000000013749, 1.517382266529735144E-13 ) ) ;
#26899=CIRCLE ( 'NONE', #68950, 15.80000000000028315 ) ;
#26989=ADVANCED_FACE ( 'NONE', ( #23430 ), #177, .F. ) ;
#27095=EDGE_LOOP ( 'NONE', ( #65715, #26183, #28952, #15973 ) ) ;
#27359=ORIENTED_EDGE ( 'NONE', *, *, #57148, .T. ) ;
#27363=ORIENTED_EDGE ( 'NONE', *, *, #52567, .T. ) ;
#27429=AXIS2_PLACEMENT_3D ( 'NONE', #12082, #35021, #6812 ) ;
#27548=CARTESIAN_POINT ( 'NONE',  ( 1.433254160131044044E-14, 1.918465386552270249E-13, 18.00000000000031974 ) ) ;
#27552=ORIENTED_EDGE ( 'NONE', *, *, #51865, .T. ) ;
#27566=CIRCLE ( 'NONE', #9541, 3.300000000000000711 ) ;
#27604=CYLINDRICAL_SURFACE ( 'NONE', #39416, 20.20000000000036522 ) ;
#27660=VERTEX_POINT ( 'NONE', #49217 ) ;
#27808=VERTEX_POINT ( 'NONE', #67631 ) ;
#27826=SHAPE_REPRESENTATION ( 'radial ball bearing_68_iso_ISO 15 RBB - 3025 - 14,SI,NC,14_68', ( #43395 ), #61521 ) ;
#27880=TOROIDAL_SURFACE ( 'NONE', #19452, 22.90000000000000213, 0.5999999999999937605 ) ;
#27887=CARTESIAN_POINT ( 'NONE',  ( -20.63749999999999218, 1.052885139195391297E-13, 12.50000000000021139 ) ) ;
#27907=ORIENTED_EDGE ( 'NONE', *, *, #5887, .T. ) ;
#27929=ORIENTED_EDGE ( 'NONE', *, *, #58551, .T. ) ;
#27981=CARTESIAN_POINT ( 'NONE',  ( -20.63749999999998863, 1.408645127833826896E-13, 15.80000000000026539 ) ) ;
#28041=DIRECTION ( 'NONE',  ( 7.962523111839282146E-16, -1.065814103640130873E-14, -1.000000000000000000 ) ) ;
#28079=CARTESIAN_POINT ( 'NONE',  ( -20.63749999999997797, 1.882991779351789328E-13, 20.20000000000035101 ) ) ;
#28194=ADVANCED_FACE ( 'NONE', ( #9926 ), #61818, .T. ) ;
#28311=CARTESIAN_POINT ( 'NONE',  ( -20.63750000000001350, -1.626958204894327051E-13, -12.50000000000024158 ) ) ;
#28328=ORIENTED_EDGE ( 'NONE', *, *, #19536, .F. ) ;
#28553=ORIENTED_EDGE ( 'NONE', *, *, #67561, .F. ) ;
#28577=EDGE_LOOP ( 'NONE', ( #44881, #27552, #60261, #62722 ) ) ;
#28915=CARTESIAN_POINT ( 'NONE',  ( 7.999999999999991118, -2.038709499516292069E-13, -20.20000000000036167 ) ) ;
#28952=ORIENTED_EDGE ( 'NONE', *, *, #60687, .T. ) ;
#29017=CARTESIAN_POINT ( 'NONE',  ( -7.400000000000003908, -1.056673655988042765E-14, -5.892267102755452808E-15 ) ) ;
#29278=CYLINDRICAL_SURFACE ( 'NONE', #73963, 15.80000000000028315 ) ;
#29383=ORIENTED_EDGE ( 'NONE', *, *, #13878, .T. ) ;
#29623=DIRECTION ( 'NONE',  ( -8.119982227976398872E-16, -1.065814103640131188E-14, -1.000000000000000000 ) ) ;
#29718=CYLINDRICAL_SURFACE ( 'NONE', #41349, 23.50000000000041922 ) ;
#29883=DIRECTION ( 'NONE',  ( 1.000000000000000000, 1.427937372958405461E-15, 7.962523111839130290E-16 ) ) ;
#29895=CIRCLE ( 'NONE', #3522, 23.50000000000041922 ) ;
#29925=ORIENTED_EDGE ( 'NONE', *, *, #12954, .T. ) ;
#29941=CIRCLE ( 'NONE', #16771, 23.50000000000041922 ) ;
#30085=DIRECTION ( 'NONE',  ( -7.632783294297813165E-16, -1.065814103640131188E-14, -1.000000000000000000 ) ) ;
#30102=DIRECTION ( 'NONE',  ( -7.685483754327489091E-16, -1.065814103640131188E-14, -1.000000000000000000 ) ) ;
#30320=( LENGTH_UNIT ( ) NAMED_UNIT ( * ) SI_UNIT ( .MILLI., .METRE. ) );
#30543=DIRECTION ( 'NONE',  ( 1.000000000000000000, 1.427937372958405461E-15, 7.962523111839130290E-16 ) ) ;
#30560=CIRCLE ( 'NONE', #69007, 3.300000000000000711 ) ;
#30585=LINE ( 'NONE', #26059, #50281 ) ;
#30669=ORIENTED_EDGE ( 'NONE', *, *, #21306, .F. ) ;
#30691=EDGE_CURVE ( 'NONE', #68921, #54538, #29941, .T. ) ;
#30739=ORIENTED_EDGE ( 'NONE', *, *, #70497, .T. ) ;
#30850=VECTOR ( 'NONE', #48829, 1000.000000000000000 ) ;
#30870=CARTESIAN_POINT ( 'NONE',  ( -7.999999999999992895, -1.142349898368590025E-14, -6.370018489464426943E-15 ) ) ;
#30937=CARTESIAN_POINT ( 'NONE',  ( -8.000000000000007105, -1.142349898368590025E-14, -6.370018489464426943E-15 ) ) ;
#31069=ORIENTED_EDGE ( 'NONE', *, *, #73348, .F. ) ;
#31219=DIRECTION ( 'NONE',  ( 0.000000000000000000, -1.065814103640136079E-14, -1.000000000000000000 ) ) ;
#31398=DIRECTION ( 'NONE',  ( 1.000000000000000000, 1.427937372958405461E-15, 7.962523111839130290E-16 ) ) ;
#31410=ADVANCED_FACE ( 'NONE', ( #21502 ), #33124, .T. ) ;
#31516=( LENGTH_UNIT ( ) NAMED_UNIT ( * ) SI_UNIT ( .MILLI., .METRE. ) );
#31536=EDGE_LOOP ( 'NONE', ( #27907, #9237, #2966, #68148 ) ) ;
#31659=CYLINDRICAL_SURFACE ( 'NONE', #65411, 15.80000000000028315 ) ;
#31750=DIRECTION ( 'NONE',  ( -8.326672684688524170E-16, -1.065814103640131188E-14, -1.000000000000000000 ) ) ;
#31937=FACE_BOUND ( 'NONE', #19882, .T. ) ;
#32065=ORIENTED_EDGE ( 'NONE', *, *, #34026, .T. ) ;
#32272=CIRCLE ( 'NONE', #73062, 3.300000000000000711 ) ;
#32390=DIRECTION ( 'NONE',  ( -8.783410004945701396E-16, -1.065814103640131188E-14, -1.000000000000000000 ) ) ;
#32423=EDGE_LOOP ( 'NONE', ( #30739, #7139 ) ) ;
#32468=DIRECTION ( 'NONE',  ( 1.000000000000000000, 1.427937372958405461E-15, 7.962523111839130290E-16 ) ) ;
#32625=FILL_AREA_STYLE ('',( #61223 ) ) ;
#32745=ADVANCED_FACE ( 'NONE', ( #44846 ), #67002, .T. ) ;
#32790=TOROIDAL_SURFACE ( 'NONE', #24442, 13.10000000000000142, 0.5999999999999998668 ) ;
#32804=ORIENTED_EDGE ( 'NONE', *, *, #49327, .T. ) ;
#32955=CIRCLE ( 'NONE', #22138, 12.50000000000022560 ) ;
#32997=VERTEX_POINT ( 'NONE', #73299 ) ;
#33093=EDGE_CURVE ( 'NONE', #59084, #23150, #8244, .T. ) ;
#33124=TOROIDAL_SURFACE ( 'NONE', #39155, 13.10000000000000142, 0.5999999999999998668 ) ;
#33155=ADVANCED_FACE ( 'NONE', ( #41328 ), #69489, .T. ) ;
#33369=ORIENTED_EDGE ( 'NONE', *, *, #8395, .F. ) ;
#33449=DIRECTION ( 'NONE',  ( -1.427937372958396981E-15, 1.000000000000000000, -1.053567635648657358E-14 ) ) ;
#33509=CYLINDRICAL_SURFACE ( 'NONE', #58644, 20.20000000000036522 ) ;
#33519=LINE ( 'NONE', #27887, #20261 ) ;
#33596=DIRECTION ( 'NONE',  ( 1.000000000000000000, 1.427937372958405461E-15, 7.962523111839130290E-16 ) ) ;
#33657=DIRECTION ( 'NONE',  ( -1.427937372958396784E-15, 1.000000000000000000, -1.078060571631604545E-14 ) ) ;
#33942=CIRCLE ( 'NONE', #48381, 15.80000000000028315 ) ;
#34026=EDGE_CURVE ( 'NONE', #44464, #73369, #27566, .T. ) ;
#34085=CARTESIAN_POINT ( 'NONE',  ( 7.999999999999994671, 1.778014505780935420E-13, 15.80000000000000426 ) ) ;
#34104=EDGE_LOOP ( 'NONE', ( #63260, #63473, #29925, #54838 ) ) ;
#34114=EDGE_LOOP ( 'NONE', ( #22686, #615, #12193, #66227 ) ) ;
#34189=EDGE_CURVE ( 'NONE', #9567, #15614, #45679, .T. ) ;
#34224=EDGE_CURVE ( 'NONE', #73310, #46312, #26435, .T. ) ;
#34384=DIRECTION ( 'NONE',  ( -8.119982227976398872E-16, -1.065814103640131188E-14, -1.000000000000000000 ) ) ;
#34392=ORIENTED_EDGE ( 'NONE', *, *, #70497, .F. ) ;
#34420=CARTESIAN_POINT ( 'NONE',  ( -7.400000000000003908, -1.056673655988042765E-14, -5.892267102755452808E-15 ) ) ;
#34452=ORIENTED_EDGE ( 'NONE', *, *, #17675, .F. ) ;
#34484=( NAMED_UNIT ( * ) PLANE_ANGLE_UNIT ( ) SI_UNIT ( $, .RADIAN. ) );
#34577=AXIS2_PLACEMENT_3D ( 'NONE', #68492, #44448, #5714 ) ;
#34625=ORIENTED_EDGE ( 'NONE', *, *, #8395, .T. ) ;
#34647=AXIS2_PLACEMENT_3D ( 'NONE', #29017, #52320, #57233 ) ;
#34680=PRODUCT_CONTEXT ( 'NONE', #15240, 'mechanical' ) ;
#34750=CIRCLE ( 'NONE', #2375, 15.80000000000028315 ) ;
#34840=ORIENTED_EDGE ( 'NONE', *, *, #54143, .T. ) ;
#34857=EDGE_CURVE ( 'NONE', #38997, #67308, #8476, .T. ) ;
#35008=CIRCLE ( 'NONE', #6198, 23.50000000000041922 ) ;
#35021=DIRECTION ( 'NONE',  ( 1.000000000000000000, 1.427937372958405461E-15, 7.962523111839130290E-16 ) ) ;
#35156=ORIENTED_EDGE ( 'NONE', *, *, #72199, .T. ) ;
#35201=ORIENTED_EDGE ( 'NONE', *, *, #63390, .T. ) ;
#35287=CARTESIAN_POINT ( 'NONE',  ( 7.400000000000003908, 1.056673655987569448E-14, 5.892267102770835596E-15 ) ) ;
#35376=DIRECTION ( 'NONE',  ( 1.000000000000000000, 1.427937372958388501E-15, -7.962523111839142123E-16 ) ) ;
#35544=CARTESIAN_POINT ( 'NONE',  ( 2.459674775249762302, 3.512261536898573354E-15, 1.958521724562357923E-15 ) ) ;
#35626=VERTEX_POINT ( 'NONE', #34085 ) ;
#35962=SURFACE_STYLE_USAGE ( .BOTH. , #58525 ) ;
#36005=ADVANCED_FACE ( 'NONE', ( #67843 ), #73444, .T. ) ;
#36042=DIRECTION ( 'NONE',  ( 0.000000000000000000, 1.053567635648656885E-14, 1.000000000000000000 ) ) ;
#36373=DIRECTION ( 'NONE',  ( 1.000000000000000000, 1.427937372958405461E-15, 7.962523111839130290E-16 ) ) ;
#36438=LINE ( 'NONE', #25901, #30850 ) ;
#36558=CARTESIAN_POINT ( 'NONE',  ( -8.000000000000007105, -1.142349898368590025E-14, -6.370018489464426943E-15 ) ) ;
#36732=ADVANCED_FACE ( 'NONE', ( #49251 ), #37030, .T. ) ;
#36742=EDGE_CURVE ( 'NONE', #45520, #53848, #25003, .T. ) ;
#36762=EDGE_CURVE ( 'NONE', #49698, #17551, #15390, .T. ) ;
#36846=PLANE ( 'NONE',  #24562 ) ;
#36913=EDGE_CURVE ( 'NONE', #62960, #60376, #9429, .T. ) ;
#36995=ADVANCED_FACE ( 'NONE', ( #25032 ), #3501, .T. ) ;
#37030=TOROIDAL_SURFACE ( 'NONE', #23825, 22.90000000000000213, 0.5999999999999937605 ) ;
#37066=AXIS2_PLACEMENT_3D ( 'NONE', #63171, #11628, #5290 ) ;
#37255=EDGE_CURVE ( 'NONE', #32997, #68921, #68605, .T. ) ;
#37271=ORIENTED_EDGE ( 'NONE', *, *, #10709, .F. ) ;
#37435=UNCERTAINTY_MEASURE_WITH_UNIT (LENGTH_MEASURE( 1.000000000000000082E-05 ), #51404, 'distance_accuracy_value', 'NONE');
#37737=DIRECTION ( 'NONE',  ( -7.632783294297813165E-16, -1.065814103640131188E-14, -1.000000000000000000 ) ) ;
#37961=PLANE ( 'NONE',  #19923 ) ;
#37980=ORIENTED_EDGE ( 'NONE', *, *, #72199, .F. ) ;
#38029=DIRECTION ( 'NONE',  ( -8.119982227976398872E-16, -1.065814103640131188E-14, -1.000000000000000000 ) ) ;
#38069=DIRECTION ( 'NONE',  ( 7.962523111839282146E-16, -1.065814103640130873E-14, -1.000000000000000000 ) ) ;
#38148=CARTESIAN_POINT ( 'NONE',  ( 0.000000000000000000, 0.000000000000000000, 0.000000000000000000 ) ) ;
#38346=CIRCLE ( 'NONE', #57578, 0.5999999999999928724 ) ;
#38997=VERTEX_POINT ( 'NONE', #25871 ) ;
#39024=( NAMED_UNIT ( * ) PLANE_ANGLE_UNIT ( ) SI_UNIT ( $, .RADIAN. ) );
#39072=CARTESIAN_POINT ( 'NONE',  ( -8.000000000000023093, -2.267179479189963121E-13, -20.20000000000037232 ) ) ;
#39155=AXIS2_PLACEMENT_3D ( 'NONE', #73379, #67381, #38069 ) ;
#39373=LINE ( 'NONE', #28079, #67861 ) ;
#39416=AXIS2_PLACEMENT_3D ( 'NONE', #16701, #17439, #50904 ) ;
#39700=FACE_OUTER_BOUND ( 'NONE', #23146, .T. ) ;
#39798=VECTOR ( 'NONE', #30543, 1000.000000000000000 ) ;
#40029=ORIENTED_EDGE ( 'NONE', *, *, #33093, .F. ) ;
#40101=AXIS2_PLACEMENT_3D ( 'NONE', #38148, #21591, #43448 ) ;
#40336=EDGE_CURVE ( 'NONE', #40700, #41879, #32272, .T. ) ;
#40508=ORIENTED_EDGE ( 'NONE', *, *, #12954, .F. ) ;
#40643=CIRCLE ( 'NONE', #52590, 0.5999999999999928724 ) ;
#40645=FACE_OUTER_BOUND ( 'NONE', #32423, .T. ) ;
#40700=VERTEX_POINT ( 'NONE', #70537 ) ;
#40717=CARTESIAN_POINT ( 'NONE',  ( 7.400000000000021672, 2.574426074635176821E-13, 22.90000000000042490 ) ) ;
#40720=DIRECTION ( 'NONE',  ( 1.000000000000000000, 1.427937372958405461E-15, 7.962523111839130290E-16 ) ) ;
#40956=DIRECTION ( 'NONE',  ( 1.000000000000000000, 1.427937372958405461E-15, 7.962523111839130290E-16 ) ) ;
#40991=AXIS2_PLACEMENT_3D ( 'NONE', #12871, #65144, #13978 ) ;
#41024=ADVANCED_FACE ( 'NONE', ( #69023 ), #67222, .T. ) ;
#41268=DIRECTION ( 'NONE',  ( 0.000000000000000000, 1.078060571631605650E-14, 1.000000000000000000 ) ) ;
#41311=CIRCLE ( 'NONE', #11312, 0.5999999999999998668 ) ;
#41328=FACE_OUTER_BOUND ( 'NONE', #31536, .T. ) ;
#41349=AXIS2_PLACEMENT_3D ( 'NONE', #5715, #843, #23003 ) ;
#41358=CARTESIAN_POINT ( 'NONE',  ( 8.000000000000007105, 1.142349898368116708E-14, 6.370018489481387452E-15 ) ) ;
#41507=CIRCLE ( 'NONE', #57094, 20.20000000000036522 ) ;
#41741=DIRECTION ( 'NONE',  ( -1.000000000000000000, -1.427937372958405461E-15, -7.962523111839130290E-16 ) ) ;
#41879=VERTEX_POINT ( 'NONE', #71861 ) ;
#42166=ORIENTED_EDGE ( 'NONE', *, *, #48056, .F. ) ;
#42281=TOROIDAL_SURFACE ( 'NONE', #60316, 13.10000000000000142, 0.5999999999999998668 ) ;
#42322=DIRECTION ( 'NONE',  ( 7.962523111839282146E-16, -1.065814103640130873E-14, -1.000000000000000000 ) ) ;
#42497=FACE_OUTER_BOUND ( 'NONE', #49802, .T. ) ;
#42643=DIRECTION ( 'NONE',  ( 0.000000000000000000, -1.065814103640131662E-14, -1.000000000000000000 ) ) ;
#42757=CARTESIAN_POINT ( 'NONE',  ( 2.459674775249762302, 3.512261536898573354E-15, 1.958521724562357923E-15 ) ) ;
#42888=DIRECTION ( 'NONE',  ( 0.000000000000000000, 1.078060571631605650E-14, 1.000000000000000000 ) ) ;
#42981=DIRECTION ( 'NONE',  ( -7.962523111838990267E-16, -1.065814103640131188E-14, -1.000000000000000000 ) ) ;
#43005=COLOUR_RGB ( '', 0.08235294, 0.09019608, 0.10196078) ;
#43320=ADVANCED_FACE ( 'NONE', ( #45567 ), #33509, .F. ) ;
#43346=DIRECTION ( 'NONE',  ( 1.000000000000000000, 1.427937372958405461E-15, 7.962523111839130290E-16 ) ) ;
#43395=AXIS2_PLACEMENT_3D ( 'NONE', #48320, #71232, #19735 ) ;
#43413=ORIENTED_EDGE ( 'NONE', *, *, #57579, .T. ) ;
#43448=DIRECTION ( 'NONE',  ( -7.962523111839282146E-16, 1.065814103640130873E-14, 1.000000000000000000 ) ) ;
#43592=ORIENTED_EDGE ( 'NONE', *, *, #14501, .F. ) ;
#43697=FACE_OUTER_BOUND ( 'NONE', #23032, .T. ) ;
#43847=CARTESIAN_POINT ( 'NONE',  ( -7.399999999999985256, 2.363091343437615473E-13, 22.90000000000041069 ) ) ;
#44025=EDGE_CURVE ( 'NONE', #14912, #53848, #33519, .T. ) ;
#44041=ORIENTED_EDGE ( 'NONE', *, *, #70616, .T. ) ;
#44137=EDGE_CURVE ( 'NONE', #54538, #62960, #2336, .T. ) ;
#44448=DIRECTION ( 'NONE',  ( 1.000000000000000000, 1.427937372958405461E-15, 7.962523111839130290E-16 ) ) ;
#44464=VERTEX_POINT ( 'NONE', #50727 ) ;
#44527=CARTESIAN_POINT ( 'NONE',  ( -20.63749999999999574, -2.946905753440916183E-14, -1.643265707205091412E-14 ) ) ;
#44594=DIRECTION ( 'NONE',  ( 0.000000000000000000, -1.065814103640131662E-14, -1.000000000000000000 ) ) ;
#44846=FACE_OUTER_BOUND ( 'NONE', #28577, .T. ) ;
#44881=ORIENTED_EDGE ( 'NONE', *, *, #62869, .F. ) ;
#44993=AXIS2_PLACEMENT_3D ( 'NONE', #59992, #59609, #42322 ) ;
#45429=ORIENTED_EDGE ( 'NONE', *, *, #44137, .F. ) ;
#45453=CARTESIAN_POINT ( 'NONE',  ( -7.400000000000021672, -2.546381662934748895E-13, -22.90000000000042490 ) ) ;
#45520=VERTEX_POINT ( 'NONE', #71436 ) ;
#45547=FACE_OUTER_BOUND ( 'NONE', #24663, .T. ) ;
#45567=FACE_OUTER_BOUND ( 'NONE', #9130, .T. ) ;
#45569=CYLINDRICAL_SURFACE ( 'NONE', #34577, 15.80000000000028315 ) ;
#45679=CIRCLE ( 'NONE', #9595, 15.80000000000028315 ) ;
#45873=CIRCLE ( 'NONE', #66306, 20.20000000000036522 ) ;
#46160=CARTESIAN_POINT ( 'NONE',  ( 7.400000000000003908, -2.398995777955595453E-13, -23.50000000000040856 ) ) ;
#46312=VERTEX_POINT ( 'NONE', #60322 ) ;
#46586=ORIENTED_EDGE ( 'NONE', *, *, #13468, .T. ) ;
#46685=CYLINDRICAL_SURFACE ( 'NONE', #15463, 12.50000000000022560 ) ;
#46788=AXIS2_PLACEMENT_3D ( 'NONE', #34420, #21662, #28041 ) ;
#46890=VERTEX_POINT ( 'NONE', #72944 ) ;
#46999=CIRCLE ( 'NONE', #56612, 20.20000000000036522 ) ;
#47014=DIRECTION ( 'NONE',  ( -1.000000000000000000, -1.427937372958388501E-15, 7.962523111839142123E-16 ) ) ;
#47081=DIRECTION ( 'NONE',  ( 1.000000000000000000, 1.427937372958405461E-15, 7.962523111839130290E-16 ) ) ;
#47128=ADVANCED_BREP_SHAPE_REPRESENTATION ( '', ( #62646, #43395 ), #61521 ) ;
#47459=EDGE_CURVE ( 'NONE', #45520, #27660, #61382, .T. ) ;
#47467=LINE ( 'NONE', #1645, #67957 ) ;
#47640=CARTESIAN_POINT ( 'NONE',  ( -7.399999999999993250, 1.306591983238623146E-13, 13.10000000000023057 ) ) ;
#47711=DIRECTION ( 'NONE',  ( 0.000000000000000000, -1.065814103640131346E-14, -1.000000000000000000 ) ) ;
#47860=AXIS2_PLACEMENT_3D ( 'NONE', #15401, #53779, #42888 ) ;
#48056=EDGE_CURVE ( 'NONE', #50841, #71000, #57780, .T. ) ;
#48212=CIRCLE ( 'NONE', #15790, 15.80000000000028315 ) ;
#48320=CARTESIAN_POINT ( 'NONE',  ( 0.000000000000000000, 0.000000000000000000, 0.000000000000000000 ) ) ;
#48381=AXIS2_PLACEMENT_3D ( 'NONE', #7169, #25197, #51641 ) ;
#48686=CARTESIAN_POINT ( 'NONE',  ( -8.000000000000019540, -1.798221273588296393E-13, -15.80000000000029026 ) ) ;
#48829=DIRECTION ( 'NONE',  ( 1.000000000000000000, 1.427937372958405461E-15, 7.962523111839130290E-16 ) ) ;
#48938=CYLINDRICAL_SURFACE ( 'NONE', #9897, 15.80000000000028315 ) ;
#48982=ADVANCED_FACE ( 'NONE', ( #2850 ), #70856, .F. ) ;
#49085=AXIS2_PLACEMENT_3D ( 'NONE', #70887, #60008, #8492 ) ;
#49217=CARTESIAN_POINT ( 'NONE',  ( 8.000000000000000000, -1.281981485932089404E-13, -13.10000000000022879 ) ) ;
#49251=FACE_OUTER_BOUND ( 'NONE', #58464, .T. ) ;
#49277=ORIENTED_EDGE ( 'NONE', *, *, #13560, .F. ) ;
#49327=EDGE_CURVE ( 'NONE', #53848, #27808, #15966, .T. ) ;
#49343=DIRECTION ( 'NONE',  ( 1.000000000000000000, 1.427937372958388501E-15, -7.962523111839142123E-16 ) ) ;
#49381=EDGE_CURVE ( 'NONE', #59117, #44464, #33942, .T. ) ;
#49526=CARTESIAN_POINT ( 'NONE',  ( -2.459674775249762302, -3.512261536895417911E-15, -1.958521724548552858E-15 ) ) ;
#49698=VERTEX_POINT ( 'NONE', #39072 ) ;
#49728=DIRECTION ( 'NONE',  ( 1.427937372958396981E-15, -1.000000000000000000, 1.065814103640131031E-14 ) ) ;
#49802=EDGE_LOOP ( 'NONE', ( #69337, #9072 ) ) ;
#49917=SURFACE_STYLE_USAGE ( .BOTH. , #4089 ) ;
#50166=EDGE_LOOP ( 'NONE', ( #7129, #1608, #26251, #49277 ) ) ;
#50172=EDGE_LOOP ( 'NONE', ( #15270, #56730, #32804, #56834 ) ) ;
#50222=EDGE_LOOP ( 'NONE', ( #28328, #4473, #32065, #63524 ) ) ;
#50233=MECHANICAL_DESIGN_GEOMETRIC_PRESENTATION_REPRESENTATION('',(#68227),#56202);
#50281=VECTOR ( 'NONE', #3168, 1000.000000000000000 ) ;
#50392=AXIS2_PLACEMENT_3D ( 'NONE', #36558, #3128, #2406 ) ;
#50514=EDGE_LOOP ( 'NONE', ( #9808, #62305 ) ) ;
#50591=ORIENTED_EDGE ( 'NONE', *, *, #63390, .F. ) ;
#50697=DIRECTION ( 'NONE',  ( 0.000000000000000000, -1.065814103640136079E-14, -1.000000000000000000 ) ) ;
#50727=CARTESIAN_POINT ( 'NONE',  ( 2.459674775249774736, 1.719108899120423124E-13, 15.80000000000028670 ) ) ;
#50729=DIRECTION ( 'NONE',  ( 1.000000000000000000, 1.427937372958405461E-15, 7.962523111839130290E-16 ) ) ;
#50804=FACE_OUTER_BOUND ( 'NONE', #34114, .T. ) ;
#50841=VERTEX_POINT ( 'NONE', #6896 ) ;
#50884=CARTESIAN_POINT ( 'NONE',  ( 8.000000000000007105, 1.142349898368116708E-14, 6.370018489481387452E-15 ) ) ;
#50904=DIRECTION ( 'NONE',  ( -8.587739980083048116E-16, -1.065814103640131346E-14, -1.000000000000000000 ) ) ;
#50919=DIRECTION ( 'NONE',  ( 1.000000000000000000, 1.427937372958405461E-15, 7.962523111839130290E-16 ) ) ;
#50978=CARTESIAN_POINT ( 'NONE',  ( 7.999999999999992895, 1.142349898368116708E-14, 6.370018489481387452E-15 ) ) ;
#51099=CARTESIAN_POINT ( 'NONE',  ( 7.400000000000003908, 1.056673655987569448E-14, 5.892267102770835596E-15 ) ) ;
#51166=ADVANCED_FACE ( 'NONE', ( #52297 ), #29718, .T. ) ;
#51261=DIRECTION ( 'NONE',  ( 1.000000000000000000, 1.427937372958405461E-15, 7.962523111839130290E-16 ) ) ;
#51286=LINE ( 'NONE', #27981, #19716 ) ;
#51404=( LENGTH_UNIT ( ) NAMED_UNIT ( * ) SI_UNIT ( .MILLI., .METRE. ) );
#51468=DIRECTION ( 'NONE',  ( -8.119982227976398872E-16, -1.065814103640131188E-14, -1.000000000000000000 ) ) ;
#51491=ADVANCED_FACE ( 'NONE', ( #62306 ), #32790, .T. ) ;
#51552=FACE_BOUND ( 'NONE', #50514, .T. ) ;
#51576=DIRECTION ( 'NONE',  ( -8.326672684688524170E-16, -1.065814103640131188E-14, -1.000000000000000000 ) ) ;
#51641=DIRECTION ( 'NONE',  ( 7.959965316982041921E-16, 1.065814103640131188E-14, 1.000000000000000000 ) ) ;
#51706=DIRECTION ( 'NONE',  ( 1.427937372958396981E-15, -1.000000000000000000, 1.065814103640131031E-14 ) ) ;
#51865=EDGE_CURVE ( 'NONE', #46312, #73310, #60517, .T. ) ;
#51933=DIRECTION ( 'NONE',  ( 1.000000000000000000, 1.427937372958405461E-15, 7.962523111839130290E-16 ) ) ;
#52010=DIRECTION ( 'NONE',  ( 1.000000000000000000, 1.427937372958405461E-15, 7.962523111839130290E-16 ) ) ;
#52137=CARTESIAN_POINT ( 'NONE',  ( -8.000000000000019540, 1.628656900575238863E-13, 15.79999999999999183 ) ) ;
#52297=FACE_OUTER_BOUND ( 'NONE', #72420, .T. ) ;
#52320=DIRECTION ( 'NONE',  ( 1.000000000000000000, 1.427937372958405461E-15, 7.962523111839130290E-16 ) ) ;
#52567=EDGE_CURVE ( 'NONE', #58263, #14912, #32955, .T. ) ;
#52590=AXIS2_PLACEMENT_3D ( 'NONE', #43847, #33657, #55483 ) ;
#52630=DIRECTION ( 'NONE',  ( 1.000000000000000000, 1.427937372958405461E-15, 7.962523111839130290E-16 ) ) ;
#52637=AXIS2_PLACEMENT_3D ( 'NONE', #14299, #8291, #3056 ) ;
#52837=DIRECTION ( 'NONE',  ( -7.945298363252408085E-16, -1.065814103640131188E-14, -1.000000000000000000 ) ) ;
#52947=DIRECTION ( 'NONE',  ( 1.000000000000000000, 1.427937372958405461E-15, 7.962523111839130290E-16 ) ) ;
#53031=CARTESIAN_POINT ( 'NONE',  ( 7.400000000000003908, 1.056673655987569448E-14, 5.892267102770835596E-15 ) ) ;
#53167=DIRECTION ( 'NONE',  ( 1.000000000000000000, 1.427937372958405461E-15, 7.962523111839130290E-16 ) ) ;
#53493=CARTESIAN_POINT ( 'NONE',  ( 2.459674775249762302, 2.188067104722127970E-13, 20.20000000000039009 ) ) ;
#53515=DIRECTION ( 'NONE',  ( -7.945298363252408085E-16, -1.065814103640131188E-14, -1.000000000000000000 ) ) ;
#53608=CLOSED_SHELL ( 'NONE', ( #6901, #28194, #36732, #43320, #26989, #33155, #31410, #13169, #51491, #69752, #55435, #36005, #36995, #392, #26635, #624, #54987, #67671, #41024, #68169, #7022, #48982, #12731, #57816, #55099, #51166, #32745, #4425 ) ) ;
#53779=DIRECTION ( 'NONE',  ( -1.427937372958396784E-15, 1.000000000000000000, -1.078060571631604545E-14 ) ) ;
#53782=DIRECTION ( 'NONE',  ( -7.632783294297813165E-16, -1.065814103640131188E-14, -1.000000000000000000 ) ) ;
#53848=VERTEX_POINT ( 'NONE', #2345 ) ;
#54065=EDGE_CURVE ( 'NONE', #27808, #53848, #69327, .T. ) ;
#54127=EDGE_LOOP ( 'NONE', ( #50591, #70743, #20954, #6929 ) ) ;
#54143=EDGE_CURVE ( 'NONE', #59084, #40700, #54940, .T. ) ;
#54150=CARTESIAN_POINT ( 'NONE',  ( -7.400000000000022560, -2.610330509153157305E-13, -23.50000000000042633 ) ) ;
#54255=AXIS2_PLACEMENT_3D ( 'NONE', #62972, #69318, #11428 ) ;
#54283=VECTOR ( 'NONE', #61504, 1000.000000000000000 ) ;
#54311=CARTESIAN_POINT ( 'NONE',  ( 7.999999999999974243, 2.611051703902955430E-13, 22.90000000000000924 ) ) ;
#54348=DIRECTION ( 'NONE',  ( -8.332732854036912157E-16, -1.065814103640131031E-14, -1.000000000000000000 ) ) ;
#54538=VERTEX_POINT ( 'NONE', #46160 ) ;
#54838=ORIENTED_EDGE ( 'NONE', *, *, #34026, .F. ) ;
#54940=CIRCLE ( 'NONE', #4520, 20.20000000000036522 ) ;
#54987=ADVANCED_FACE ( 'NONE', ( #39700 ), #42281, .T. ) ;
#55099=ADVANCED_FACE ( 'NONE', ( #11836 ), #27880, .T. ) ;
#55435=ADVANCED_FACE ( 'NONE', ( #43697 ), #48938, .T. ) ;
#55483=DIRECTION ( 'NONE',  ( 0.000000000000000000, 1.078060571631605808E-14, 1.000000000000000000 ) ) ;
#55558=AXIS2_PLACEMENT_3D ( 'NONE', #50978, #5136, #57004 ) ;
#55621=DIRECTION ( 'NONE',  ( -1.000000000000000000, -1.427937372958388501E-15, 7.962523111839142123E-16 ) ) ;
#55961=EDGE_LOOP ( 'NONE', ( #73684, #69554, #6758, #10202 ) ) ;
#56202=( GEOMETRIC_REPRESENTATION_CONTEXT ( 3 ) GLOBAL_UNCERTAINTY_ASSIGNED_CONTEXT ( ( #71413 ) ) GLOBAL_UNIT_ASSIGNED_CONTEXT ( ( #30320, #34484, #23225 ) ) REPRESENTATION_CONTEXT ( 'NONE', 'WORKASPACE' ) );
#56275=CIRCLE ( 'NONE', #27429, 15.80000000000028315 ) ;
#56363=CARTESIAN_POINT ( 'NONE',  ( -8.000000000000007105, -1.142349898368590025E-14, -6.370018489464426943E-15 ) ) ;
#56376=CARTESIAN_POINT ( 'NONE',  ( 2.459674775249762302, -2.093084008641303565E-13, -20.20000000000035456 ) ) ;
#56378=AXIS2_PLACEMENT_3D ( 'NONE', #40717, #57269, #23789 ) ;
#56586=DIRECTION ( 'NONE',  ( 1.000000000000000000, 1.427937372958405461E-15, 7.962523111839130290E-16 ) ) ;
#56612=AXIS2_PLACEMENT_3D ( 'NONE', #50884, #22701, #57276 ) ;
#56730=ORIENTED_EDGE ( 'NONE', *, *, #44025, .T. ) ;
#56781=ORIENTED_EDGE ( 'NONE', *, *, #60522, .T. ) ;
#56798=ORIENTED_EDGE ( 'NONE', *, *, #68598, .T. ) ;
#56834=ORIENTED_EDGE ( 'NONE', *, *, #60522, .F. ) ;
#56863=PRODUCT_DEFINITION ( 'UNKNOWN', '', #12394, #70960 ) ;
#56910=CARTESIAN_POINT ( 'NONE',  ( -20.63749999999999574, -2.946905753440916183E-14, -1.643265707205091412E-14 ) ) ;
#56980=CARTESIAN_POINT ( 'NONE',  ( -20.63750000000001350, -2.447635064697195611E-13, -20.20000000000038298 ) ) ;
#57004=DIRECTION ( 'NONE',  ( -8.332732854036912157E-16, -1.065814103640131031E-14, -1.000000000000000000 ) ) ;
#57094=AXIS2_PLACEMENT_3D ( 'NONE', #35544, #58116, #74294 ) ;
#57148=EDGE_CURVE ( 'NONE', #15614, #9567, #26899, .T. ) ;
#57233=DIRECTION ( 'NONE',  ( 7.962523111839282146E-16, -1.065814103640130873E-14, -1.000000000000000000 ) ) ;
#57241=CIRCLE ( 'NONE', #825, 0.5999999999999998668 ) ;
#57269=DIRECTION ( 'NONE',  ( -1.427937372958396784E-15, 1.000000000000000000, -1.078060571631604545E-14 ) ) ;
#57276=DIRECTION ( 'NONE',  ( -7.728965982074743403E-16, -1.065814103640131188E-14, -1.000000000000000000 ) ) ;
#57326=CARTESIAN_POINT ( 'NONE',  ( -7.400000000000003908, -1.056673655988042765E-14, -5.892267102755452808E-15 ) ) ;
#57578=AXIS2_PLACEMENT_3D ( 'NONE', #45453, #69116, #50697 ) ;
#57579=EDGE_CURVE ( 'NONE', #44464, #35626, #51286, .T. ) ;
#57728=CARTESIAN_POINT ( 'NONE',  ( 7.400000000000003908, 1.056673655987569448E-14, 5.892267102770835596E-15 ) ) ;
#57780=CIRCLE ( 'NONE', #40991, 20.20000000000036522 ) ;
#57816=ADVANCED_FACE ( 'NONE', ( #21133, #3509 ), #26414, .T. ) ;
#57964=DIRECTION ( 'NONE',  ( 1.000000000000000000, 1.427937372958405461E-15, 7.962523111839130290E-16 ) ) ;
#58116=DIRECTION ( 'NONE',  ( 1.000000000000000000, 1.427937372958405461E-15, 7.962523111839130290E-16 ) ) ;
#58162=FILL_AREA_STYLE ('',( #17567 ) ) ;
#58263=VERTEX_POINT ( 'NONE', #4815 ) ;
#58464=EDGE_LOOP ( 'NONE', ( #15407, #35201, #13130, #45429 ) ) ;
#58525=SURFACE_SIDE_STYLE ('',( #12658 ) ) ;
#58551=EDGE_CURVE ( 'NONE', #73369, #50841, #39373, .T. ) ;
#58644=AXIS2_PLACEMENT_3D ( 'NONE', #68860, #68109, #5344 ) ;
#59066=DIRECTION ( 'NONE',  ( 1.427937372958396981E-15, -1.000000000000000000, 1.065814103640131031E-14 ) ) ;
#59084=VERTEX_POINT ( 'NONE', #72312 ) ;
#59117=VERTEX_POINT ( 'NONE', #62541 ) ;
#59144=CARTESIAN_POINT ( 'NONE',  ( 2.459674775249762302, 3.512261536898573354E-15, 1.958521724562357923E-15 ) ) ;
#59288=ORIENTED_EDGE ( 'NONE', *, *, #14501, .T. ) ;
#59441=EDGE_CURVE ( 'NONE', #15614, #41879, #18862, .T. ) ;
#59609=DIRECTION ( 'NONE',  ( 1.000000000000000000, 1.427937372958405461E-15, 7.962523111839130290E-16 ) ) ;
#59613=CIRCLE ( 'NONE', #23593, 20.20000000000036522 ) ;
#59673=ORIENTED_EDGE ( 'NONE', *, *, #36742, .F. ) ;
#59743=DIRECTION ( 'NONE',  ( 1.427937372958396981E-15, -1.000000000000000000, 1.065814103640131031E-14 ) ) ;
#59795=DIRECTION ( 'NONE',  ( -7.962523111838990267E-16, -1.065814103640131188E-14, -1.000000000000000000 ) ) ;
#59992=CARTESIAN_POINT ( 'NONE',  ( -7.400000000000003908, -1.056673655988042765E-14, -5.892267102755452808E-15 ) ) ;
#60008=DIRECTION ( 'NONE',  ( -1.000000000000000000, -1.427937372958405461E-15, -7.962523111839130290E-16 ) ) ;
#60068=AXIS2_PLACEMENT_3D ( 'NONE', #30870, #65114, #60582 ) ;
#60071=DIRECTION ( 'NONE',  ( 7.959965316982041921E-16, 1.065814103640131188E-14, 1.000000000000000000 ) ) ;
#60099=DIRECTION ( 'NONE',  ( 1.000000000000000000, 1.427937372958405461E-15, 7.962523111839130290E-16 ) ) ;
#60142=VECTOR ( 'NONE', #24189, 1000.000000000000000 ) ;
#60191=CARTESIAN_POINT ( 'NONE',  ( -7.400000000000003908, -1.056673655988042765E-14, -5.892267102755452808E-15 ) ) ;
#60261=ORIENTED_EDGE ( 'NONE', *, *, #10709, .T. ) ;
#60310=DIRECTION ( 'NONE',  ( 1.000000000000000000, 1.427937372958405461E-15, 7.962523111839130290E-16 ) ) ;
#60315=ORIENTED_EDGE ( 'NONE', *, *, #58551, .F. ) ;
#60316=AXIS2_PLACEMENT_3D ( 'NONE', #22780, #69006, #67890 ) ;
#60322=CARTESIAN_POINT ( 'NONE',  ( -8.000000000000012434, 2.391149348467643667E-13, 22.89999999999999503 ) ) ;
#60329=ORIENTED_EDGE ( 'NONE', *, *, #70616, .F. ) ;
#60376=VERTEX_POINT ( 'NONE', #54311 ) ;
#60517=CIRCLE ( 'NONE', #68944, 22.90000000000041780 ) ;
#60522=EDGE_CURVE ( 'NONE', #58263, #27808, #21560, .T. ) ;
#60582=DIRECTION ( 'NONE',  ( -8.332732854036912157E-16, -1.065814103640131031E-14, -1.000000000000000000 ) ) ;
#60687=EDGE_CURVE ( 'NONE', #59117, #46890, #47467, .T. ) ;
#60971=CARTESIAN_POINT ( 'NONE',  ( -20.63750000000000284, -2.946905753441389499E-14, -1.643265707204933640E-14 ) ) ;
#61073=AXIS2_PLACEMENT_3D ( 'NONE', #72899, #50729, #61654 ) ;
#61223=FILL_AREA_STYLE_COLOUR ( '', #3888 ) ;
#61331=CIRCLE ( 'NONE', #140, 13.10000000000023590 ) ;
#61382=CIRCLE ( 'NONE', #20531, 13.10000000000023590 ) ;
#61504=DIRECTION ( 'NONE',  ( 1.000000000000000000, 1.427937372958405461E-15, 7.962523111839130290E-16 ) ) ;
#61521=( GEOMETRIC_REPRESENTATION_CONTEXT ( 3 ) GLOBAL_UNCERTAINTY_ASSIGNED_CONTEXT ( ( #71990 ) ) GLOBAL_UNIT_ASSIGNED_CONTEXT ( ( #31516, #14223, #65742 ) ) REPRESENTATION_CONTEXT ( 'NONE', 'WORKASPACE' ) );
#61617=TOROIDAL_SURFACE ( 'NONE', #44993, 22.90000000000000213, 0.5999999999999937605 ) ;
#61654=DIRECTION ( 'NONE',  ( -8.332732854036912157E-16, -1.065814103640131031E-14, -1.000000000000000000 ) ) ;
#61662=TOROIDAL_SURFACE ( 'NONE', #40101, 18.00000000000000000, 3.300000000000000266 ) ;
#61670=CARTESIAN_POINT ( 'NONE',  ( -1.433254160131044044E-14, -1.896421744167617418E-13, -18.00000000000031974 ) ) ;
#61818=CYLINDRICAL_SURFACE ( 'NONE', #15357, 23.50000000000041922 ) ;
#61951=VECTOR ( 'NONE', #32468, 1000.000000000000000 ) ;
#61961=( NAMED_UNIT ( * ) SI_UNIT ( $, .STERADIAN. ) SOLID_ANGLE_UNIT ( ) );
#62305=ORIENTED_EDGE ( 'NONE', *, *, #47459, .F. ) ;
#62306=FACE_OUTER_BOUND ( 'NONE', #55961, .T. ) ;
#62533=CARTESIAN_POINT ( 'NONE',  ( -2.459674775249762302, -3.512261536895417911E-15, -1.958521724548552858E-15 ) ) ;
#62541=CARTESIAN_POINT ( 'NONE',  ( 2.459674775249774736, -1.861299128798561507E-13, -15.79999999999999538 ) ) ;
#62646=MANIFOLD_SOLID_BREP ( 'OuterRace', #53608 ) ;
#62722=ORIENTED_EDGE ( 'NONE', *, *, #13468, .F. ) ;
#62748=AXIS2_PLACEMENT_3D ( 'NONE', #25744, #2117, #71591 ) ;
#62869=EDGE_CURVE ( 'NONE', #46312, #32997, #40643, .T. ) ;
#62960=VERTEX_POINT ( 'NONE', #63007 ) ;
#62972=CARTESIAN_POINT ( 'NONE',  ( 0.000000000000000000, 0.000000000000000000, 0.000000000000000000 ) ) ;
#63007=CARTESIAN_POINT ( 'NONE',  ( 7.999999999999974243, -2.326479307499132695E-13, -22.90000000000041069 ) ) ;
#63171=CARTESIAN_POINT ( 'NONE',  ( 0.000000000000000000, 0.000000000000000000, 0.000000000000000000 ) ) ;
#63260=ORIENTED_EDGE ( 'NONE', *, *, #7663, .T. ) ;
#63382=CARTESIAN_POINT ( 'NONE',  ( 8.000000000000007105, 1.142349898368116708E-14, 6.370018489481387452E-15 ) ) ;
#63390=EDGE_CURVE ( 'NONE', #68921, #60376, #69565, .T. ) ;
#63473=ORIENTED_EDGE ( 'NONE', *, *, #19536, .T. ) ;
#63524=ORIENTED_EDGE ( 'NONE', *, *, #67561, .T. ) ;
#63552=ORIENTED_EDGE ( 'NONE', *, *, #4336, .F. ) ;
#63575=AXIS2_PLACEMENT_3D ( 'NONE', #15527, #67778, #73399 ) ;
#63665=DIRECTION ( 'NONE',  ( -8.587739980083048116E-16, -1.065814103640131346E-14, -1.000000000000000000 ) ) ;
#63924=EDGE_LOOP ( 'NONE', ( #6504, #21078, #63552, #37271 ) ) ;
#64002=CIRCLE ( 'NONE', #55558, 22.90000000000041780 ) ;
#64253=CARTESIAN_POINT ( 'NONE',  ( -20.63750000000000284, -2.946905753441389499E-14, -1.643265707204933640E-14 ) ) ;
#64567=CARTESIAN_POINT ( 'NONE',  ( -7.400000000000013678, 1.347575714539655834E-13, 12.49999999999999467 ) ) ;
#65069=CARTESIAN_POINT ( 'NONE',  ( 8.000000000000007105, 13.10000000000016485, 1.604118440328575499E-13 ) ) ;
#65114=DIRECTION ( 'NONE',  ( 1.000000000000000000, 1.427937372958405461E-15, 7.962523111839130290E-16 ) ) ;
#65144=DIRECTION ( 'NONE',  ( 1.000000000000000000, 1.427937372958405461E-15, 7.962523111839130290E-16 ) ) ;
#65190=EDGE_CURVE ( 'NONE', #27660, #45520, #61331, .T. ) ;
#65202=CARTESIAN_POINT ( 'NONE',  ( 7.400000000000003908, 1.056673655987569448E-14, 5.892267102770835596E-15 ) ) ;
#65325=CIRCLE ( 'NONE', #14916, 15.80000000000028315 ) ;
#65411=AXIS2_PLACEMENT_3D ( 'NONE', #21482, #43346, #15481 ) ;
#65691=DIRECTION ( 'NONE',  ( -1.000000000000000000, -1.427937372958405461E-15, -7.962523111839130290E-16 ) ) ;
#65715=ORIENTED_EDGE ( 'NONE', *, *, #57579, .F. ) ;
#65742=( NAMED_UNIT ( * ) SI_UNIT ( $, .STERADIAN. ) SOLID_ANGLE_UNIT ( ) );
#65946=EDGE_CURVE ( 'NONE', #71000, #50841, #46999, .T. ) ;
#66104=DIRECTION ( 'NONE',  ( -7.959965316982041921E-16, -1.065814103640131188E-14, -1.000000000000000000 ) ) ;
#66165=DIRECTION ( 'NONE',  ( 1.000000000000000000, 1.427937372958405461E-15, 7.962523111839130290E-16 ) ) ;
#66202=APPLICATION_CONTEXT ( 'automotive_design' ) ;
#66227=ORIENTED_EDGE ( 'NONE', *, *, #22061, .F. ) ;
#66306=AXIS2_PLACEMENT_3D ( 'NONE', #56363, #66165, #10112 ) ;
#66378=AXIS2_PLACEMENT_3D ( 'NONE', #53031, #51261, #30085 ) ;
#66606=CARTESIAN_POINT ( 'NONE',  ( -7.400000000000003908, -1.056673655988042765E-14, -5.892267102755452808E-15 ) ) ;
#66963=DIRECTION ( 'NONE',  ( 1.000000000000000000, 1.427937372958405461E-15, 7.962523111839130290E-16 ) ) ;
#67002=TOROIDAL_SURFACE ( 'NONE', #34647, 22.90000000000000213, 0.5999999999999937605 ) ;
#67205=ORIENTED_EDGE ( 'NONE', *, *, #49327, .F. ) ;
#67222=TOROIDAL_SURFACE ( 'NONE', #46788, 13.10000000000000142, 0.5999999999999998668 ) ;
#67308=VERTEX_POINT ( 'NONE', #14552 ) ;
#67381=DIRECTION ( 'NONE',  ( 1.000000000000000000, 1.427937372958405461E-15, 7.962523111839130290E-16 ) ) ;
#67561=EDGE_CURVE ( 'NONE', #73369, #68357, #41507, .T. ) ;
#67631=CARTESIAN_POINT ( 'NONE',  ( 7.399999999999994138, -1.226600263951431156E-13, -12.50000000000022027 ) ) ;
#67671=ADVANCED_FACE ( 'NONE', ( #14834 ), #25389, .F. ) ;
#67778=DIRECTION ( 'NONE',  ( 1.000000000000000000, 1.427937372958405461E-15, 7.962523111839130290E-16 ) ) ;
#67843=FACE_OUTER_BOUND ( 'NONE', #34104, .T. ) ;
#67861=VECTOR ( 'NONE', #10800, 1000.000000000000000 ) ;
#67890=DIRECTION ( 'NONE',  ( 7.962523111839282146E-16, -1.065814103640130873E-14, -1.000000000000000000 ) ) ;
#67957=VECTOR ( 'NONE', #68924, 1000.000000000000000 ) ;
#68109=DIRECTION ( 'NONE',  ( 1.000000000000000000, 1.427937372958405461E-15, 7.962523111839130290E-16 ) ) ;
#68148=ORIENTED_EDGE ( 'NONE', *, *, #40336, .F. ) ;
#68169=ADVANCED_FACE ( 'NONE', ( #31937, #42497 ), #37961, .T. ) ;
#68227=STYLED_ITEM ( 'NONE', ( #7406 ), #62646 ) ;
#68357=VERTEX_POINT ( 'NONE', #56376 ) ;
#68492=CARTESIAN_POINT ( 'NONE',  ( -20.63750000000000284, -2.946905753441389499E-14, -1.643265707204933640E-14 ) ) ;
#68598=EDGE_CURVE ( 'NONE', #27660, #27808, #57241, .T. ) ;
#68605=LINE ( 'NONE', #16726, #70700 ) ;
#68860=CARTESIAN_POINT ( 'NONE',  ( -20.63749999999999574, -2.946905753440916183E-14, -1.643265707205091412E-14 ) ) ;
#68899=DIRECTION ( 'NONE',  ( -7.685483754327489091E-16, -1.065814103640131188E-14, -1.000000000000000000 ) ) ;
#68921=VERTEX_POINT ( 'NONE', #73919 ) ;
#68924=DIRECTION ( 'NONE',  ( 1.000000000000000000, 1.427937372958405461E-15, 7.962523111839130290E-16 ) ) ;
#68941=CARTESIAN_POINT ( 'NONE',  ( -20.63749999999997797, 1.882991779351789328E-13, 20.20000000000035101 ) ) ;
#68944=AXIS2_PLACEMENT_3D ( 'NONE', #14102, #31398, #54348 ) ;
#68950=AXIS2_PLACEMENT_3D ( 'NONE', #70302, #18806, #1944 ) ;
#69006=DIRECTION ( 'NONE',  ( 1.000000000000000000, 1.427937372958405461E-15, 7.962523111839130290E-16 ) ) ;
#69007=AXIS2_PLACEMENT_3D ( 'NONE', #19483, #6740, #36042 ) ;
#69023=FACE_OUTER_BOUND ( 'NONE', #18687, .T. ) ;
#69111=ORIENTED_EDGE ( 'NONE', *, *, #37255, .F. ) ;
#69116=DIRECTION ( 'NONE',  ( 1.427937372958396981E-15, -1.000000000000000000, 1.065814103640131031E-14 ) ) ;
#69251=AXIS2_PLACEMENT_3D ( 'NONE', #56910, #40720, #63665 ) ;
#69318=DIRECTION ( 'NONE',  ( -1.000000000000000000, -1.427937372958405461E-15, -7.962523111839130290E-16 ) ) ;
#69327=CIRCLE ( 'NONE', #70486, 12.50000000000022560 ) ;
#69337=ORIENTED_EDGE ( 'NONE', *, *, #34189, .F. ) ;
#69489=TOROIDAL_SURFACE ( 'NONE', #37066, 18.00000000000000000, 3.300000000000000266 ) ;
#69554=ORIENTED_EDGE ( 'NONE', *, *, #36742, .T. ) ;
#69565=CIRCLE ( 'NONE', #56378, 0.5999999999999928724 ) ;
#69566=DIRECTION ( 'NONE',  ( 7.962523111838990267E-16, 1.065814103640131188E-14, 1.000000000000000000 ) ) ;
#69752=ADVANCED_FACE ( 'NONE', ( #50804 ), #45569, .T. ) ;
#69912=ORIENTED_EDGE ( 'NONE', *, *, #65946, .F. ) ;
#70026=LINE ( 'NONE', #68941, #60142 ) ;
#70083=CARTESIAN_POINT ( 'NONE',  ( -2.459674775249774736, -1.719108899120391569E-13, -15.80000000000028670 ) ) ;
#70302=CARTESIAN_POINT ( 'NONE',  ( -8.000000000000007105, -1.142349898368590025E-14, -6.370018489464426943E-15 ) ) ;
#70486=AXIS2_PLACEMENT_3D ( 'NONE', #65202, #60310, #37737 ) ;
#70497=EDGE_CURVE ( 'NONE', #46890, #35626, #15474, .T. ) ;
#70537=CARTESIAN_POINT ( 'NONE',  ( -2.459674775249762302, 2.117821873984080520E-13, 20.20000000000035456 ) ) ;
#70616=EDGE_CURVE ( 'NONE', #41879, #23150, #56275, .T. ) ;
#70700=VECTOR ( 'NONE', #56586, 1000.000000000000000 ) ;
#70743=ORIENTED_EDGE ( 'NONE', *, *, #30691, .T. ) ;
#70856=CYLINDRICAL_SURFACE ( 'NONE', #62748, 20.20000000000036522 ) ;
#70872=FACE_OUTER_BOUND ( 'NONE', #63924, .T. ) ;
#70887=CARTESIAN_POINT ( 'NONE',  ( 0.000000000000000000, 0.000000000000000000, 0.000000000000000000 ) ) ;
#70960=PRODUCT_DEFINITION_CONTEXT ( 'detailed design', #66202, 'design' ) ;
#71000=VERTEX_POINT ( 'NONE', #28915 ) ;
#71046=DIRECTION ( 'NONE',  ( 7.962523111838990267E-16, 1.065814103640131188E-14, 1.000000000000000000 ) ) ;
#71189=DIRECTION ( 'NONE',  ( 1.427937372958396981E-15, -1.000000000000000000, 1.065814103640131031E-14 ) ) ;
#71220=EDGE_CURVE ( 'NONE', #23150, #41879, #34750, .T. ) ;
#71232=DIRECTION ( 'NONE',  ( 0.000000000000000000, 0.000000000000000000, 1.000000000000000000 ) ) ;
#71368=ORIENTED_EDGE ( 'NONE', *, *, #44025, .F. ) ;
#71413=UNCERTAINTY_MEASURE_WITH_UNIT (LENGTH_MEASURE( 1.000000000000000082E-05 ), #30320, 'distance_accuracy_value', 'NONE');
#71436=CARTESIAN_POINT ( 'NONE',  ( 8.000000000000021316, 1.526494338673934908E-13, 13.10000000000024301 ) ) ;
#71457=ORIENTED_EDGE ( 'NONE', *, *, #52567, .F. ) ;
#71591=DIRECTION ( 'NONE',  ( -8.587739980083048116E-16, -1.065814103640131346E-14, -1.000000000000000000 ) ) ;
#71842=EDGE_LOOP ( 'NONE', ( #71368, #71457, #56781, #19586 ) ) ;
#71861=CARTESIAN_POINT ( 'NONE',  ( -2.459674775249774736, 1.628656900575240630E-13, 15.79999999999999538 ) ) ;
#71916=ORIENTED_EDGE ( 'NONE', *, *, #59441, .F. ) ;
#71972=CARTESIAN_POINT ( 'NONE',  ( -20.63750000000000284, -2.946905753441389499E-14, -1.643265707204933640E-14 ) ) ;
#71990=UNCERTAINTY_MEASURE_WITH_UNIT (LENGTH_MEASURE( 1.000000000000000082E-05 ), #31516, 'distance_accuracy_value', 'NONE');
#72199=EDGE_CURVE ( 'NONE', #14912, #38997, #20474, .T. ) ;
#72312=CARTESIAN_POINT ( 'NONE',  ( -2.459674775249762302, -2.163329239379351016E-13, -20.20000000000039009 ) ) ;
#72420=EDGE_LOOP ( 'NONE', ( #69111, #46586, #7225, #26064 ) ) ;
#72776=PRODUCT ( 'radial ball bearing_68_iso_ISO 15 RBB - 3025 - 14,SI,NC,14_68', 'radial ball bearing_68_iso_ISO 15 RBB - 3025 - 14,SI,NC,14_68', '', ( #34680 ) ) ;
#72835=PRESENTATION_STYLE_ASSIGNMENT (( #49917 ) ) ;
#72899=CARTESIAN_POINT ( 'NONE',  ( 7.999999999999992895, 1.142349898368116708E-14, 6.370018489481387452E-15 ) ) ;
#72944=CARTESIAN_POINT ( 'NONE',  ( 7.999999999999994671, -1.569751293914625593E-13, -15.80000000000027605 ) ) ;
#73062=AXIS2_PLACEMENT_3D ( 'NONE', #19505, #59743, #47711 ) ;
#73195=ORIENTED_EDGE ( 'NONE', *, *, #21306, .T. ) ;
#73299=CARTESIAN_POINT ( 'NONE',  ( -7.400000000000022560, 2.533442343334467755E-13, 23.49999999999998934 ) ) ;
#73310=VERTEX_POINT ( 'NONE', #23810 ) ;
#73348=EDGE_CURVE ( 'NONE', #67308, #38997, #8393, .T. ) ;
#73369=VERTEX_POINT ( 'NONE', #53493 ) ;
#73379=CARTESIAN_POINT ( 'NONE',  ( -7.400000000000003908, -1.056673655988042765E-14, -5.892267102755452808E-15 ) ) ;
#73399=DIRECTION ( 'NONE',  ( -7.632783294297813165E-16, -1.065814103640131188E-14, -1.000000000000000000 ) ) ;
#73406=DIRECTION ( 'NONE',  ( -7.943659481576819828E-16, -1.065814103640131188E-14, -1.000000000000000000 ) ) ;
#73444=TOROIDAL_SURFACE ( 'NONE', #54255, 18.00000000000000000, 3.300000000000000266 ) ;
#73467=( GEOMETRIC_REPRESENTATION_CONTEXT ( 3 ) GLOBAL_UNCERTAINTY_ASSIGNED_CONTEXT ( ( #37435 ) ) GLOBAL_UNIT_ASSIGNED_CONTEXT ( ( #51404, #39024, #61961 ) ) REPRESENTATION_CONTEXT ( 'NONE', 'WORKASPACE' ) );
#73684=ORIENTED_EDGE ( 'NONE', *, *, #65190, .T. ) ;
#73814=DIRECTION ( 'NONE',  ( -7.381802025433090153E-16, -1.065814103640131188E-14, -1.000000000000000000 ) ) ;
#73919=CARTESIAN_POINT ( 'NONE',  ( 7.400000000000003908, 2.639109708933072986E-13, 23.50000000000042277 ) ) ;
#73963=AXIS2_PLACEMENT_3D ( 'NONE', #64253, #40956, #34 ) ;
#74023=DIRECTION ( 'NONE',  ( 1.000000000000000000, 1.427937372958405461E-15, 7.962523111839130290E-16 ) ) ;
#74292=AXIS2_PLACEMENT_3D ( 'NONE', #59144, #52010, #23453 ) ;
#74294=DIRECTION ( 'NONE',  ( 7.943659481576819828E-16, 1.065814103640131188E-14, 1.000000000000000000 ) ) ;
ENDSEC;
END-ISO-10303-21;
